ISO-10303-21;
HEADER;
/* Generated by software containing ST-Developer
 * from STEP Tools, Inc. (www.steptools.com) 
 */

FILE_DESCRIPTION(
/* description */ ('Independent Whitworth quick-return mechanism. Crank radius40, ground-
center spacing80, lever180, connecting rod160, output guide X200. Nomi
nal stroke180 and long/short phase ratio2. Retained guide rods, replac
eable bearing sleeves and captured sliding shoe. No load or production
 rating assigned.'),
/* implementation_level */ '2;1');

FILE_NAME(
/* name */ 'Pivot washer.step',
/* time_stamp */ '2026-11-09T18:22:56-08:00',
/* author */ (''),
/* organization */ (''),
/* preprocessor_version */ 'ST-DEVELOPER v20.2',
/* originating_system */ 'Autodesk Translation Framework v15.17.0.0',
/* authorisation */ '');

FILE_SCHEMA (('AUTOMOTIVE_DESIGN { 1 0 10303 214 3 1 1 }'));
ENDSEC;

DATA;
#10=MECHANICAL_DESIGN_GEOMETRIC_PRESENTATION_REPRESENTATION('',(#237),#4388);
#197=SHAPE_REPRESENTATION_RELATIONSHIP('SRR','None',#4496,#217);
#217=ADVANCED_BREP_SHAPE_REPRESENTATION('',(#257),#4386);
#237=STYLED_ITEM('',(#4598),#257);
#257=MANIFOLD_SOLID_BREP('Body1',#2342);
#317=FACE_BOUND('',#750,.T.);
#318=FACE_BOUND('',#752,.T.);
#399=PLANE('',#2842);
#400=PLANE('',#2843);
#542=FACE_OUTER_BOUND('',#747,.T.);
#543=FACE_OUTER_BOUND('',#748,.T.);
#544=FACE_OUTER_BOUND('',#749,.T.);
#545=FACE_OUTER_BOUND('',#751,.T.);
#747=EDGE_LOOP('',(#2080,#2081,#2082,#2083));
#748=EDGE_LOOP('',(#2084,#2085,#2086,#2087));
#749=EDGE_LOOP('',(#2088));
#750=EDGE_LOOP('',(#2089));
#751=EDGE_LOOP('',(#2090));
#752=EDGE_LOOP('',(#2091));
#888=LINE('',#4266,#1027);
#889=LINE('',#4272,#1028);
#1027=VECTOR('',#3572,5.);
#1028=VECTOR('',#3579,10.);
#1151=CIRCLE('',#2837,5.);
#1152=CIRCLE('',#2838,5.);
#1153=CIRCLE('',#2840,10.);
#1154=CIRCLE('',#2841,10.);
#1321=VERTEX_POINT('',#4263);
#1322=VERTEX_POINT('',#4265);
#1323=VERTEX_POINT('',#4269);
#1324=VERTEX_POINT('',#4271);
#1576=EDGE_CURVE('',#1321,#1321,#1151,.T.);
#1577=EDGE_CURVE('',#1321,#1322,#888,.T.);
#1578=EDGE_CURVE('',#1322,#1322,#1152,.T.);
#1579=EDGE_CURVE('',#1323,#1323,#1153,.T.);
#1580=EDGE_CURVE('',#1323,#1324,#889,.T.);
#1581=EDGE_CURVE('',#1324,#1324,#1154,.T.);
#2080=ORIENTED_EDGE('',*,*,#1576,.F.);
#2081=ORIENTED_EDGE('',*,*,#1577,.T.);
#2082=ORIENTED_EDGE('',*,*,#1578,.T.);
#2083=ORIENTED_EDGE('',*,*,#1577,.F.);
#2084=ORIENTED_EDGE('',*,*,#1579,.F.);
#2085=ORIENTED_EDGE('',*,*,#1580,.T.);
#2086=ORIENTED_EDGE('',*,*,#1581,.T.);
#2087=ORIENTED_EDGE('',*,*,#1580,.F.);
#2088=ORIENTED_EDGE('',*,*,#1579,.T.);
#2089=ORIENTED_EDGE('',*,*,#1576,.T.);
#2090=ORIENTED_EDGE('',*,*,#1581,.F.);
#2091=ORIENTED_EDGE('',*,*,#1578,.F.);
#2173=CYLINDRICAL_SURFACE('',#2836,5.);
#2174=CYLINDRICAL_SURFACE('',#2839,10.);
#2314=ADVANCED_FACE('',(#542),#2173,.F.);
#2315=ADVANCED_FACE('',(#543),#2174,.T.);
#2316=ADVANCED_FACE('',(#544,#317),#399,.T.);
#2317=ADVANCED_FACE('',(#545,#318),#400,.F.);
#2342=CLOSED_SHELL('',(#2314,#2315,#2316,#2317));
#2835=AXIS2_PLACEMENT_3D('',#4261,#3566,#3567);
#2836=AXIS2_PLACEMENT_3D('',#4262,#3568,#3569);
#2837=AXIS2_PLACEMENT_3D('',#4264,#3570,#3571);
#2838=AXIS2_PLACEMENT_3D('',#4267,#3573,#3574);
#2839=AXIS2_PLACEMENT_3D('',#4268,#3575,#3576);
#2840=AXIS2_PLACEMENT_3D('',#4270,#3577,#3578);
#2841=AXIS2_PLACEMENT_3D('',#4273,#3580,#3581);
#2842=AXIS2_PLACEMENT_3D('',#4274,#3582,#3583);
#2843=AXIS2_PLACEMENT_3D('',#4275,#3584,#3585);
#3566=DIRECTION('axis',(0.,0.,1.));
#3567=DIRECTION('refdir',(1.,0.,0.));
#3568=DIRECTION('center_axis',(0.,0.,1.));
#3569=DIRECTION('ref_axis',(1.,0.,0.));
#3570=DIRECTION('center_axis',(0.,0.,-1.));
#3571=DIRECTION('ref_axis',(1.,0.,0.));
#3572=DIRECTION('',(0.,0.,-1.));
#3573=DIRECTION('center_axis',(0.,0.,-1.));
#3574=DIRECTION('ref_axis',(1.,0.,0.));
#3575=DIRECTION('center_axis',(0.,0.,1.));
#3576=DIRECTION('ref_axis',(1.,0.,0.));
#3577=DIRECTION('center_axis',(0.,0.,1.));
#3578=DIRECTION('ref_axis',(1.,0.,0.));
#3579=DIRECTION('',(0.,0.,-1.));
#3580=DIRECTION('center_axis',(0.,0.,1.));
#3581=DIRECTION('ref_axis',(1.,0.,0.));
#3582=DIRECTION('center_axis',(0.,0.,1.));
#3583=DIRECTION('ref_axis',(1.,0.,0.));
#3584=DIRECTION('center_axis',(0.,0.,1.));
#3585=DIRECTION('ref_axis',(1.,0.,0.));
#4261=CARTESIAN_POINT('',(0.,0.,0.));
#4262=CARTESIAN_POINT('Origin',(0.,0.,0.));
#4263=CARTESIAN_POINT('',(-5.,-6.12323399573677E-16,2.));
#4264=CARTESIAN_POINT('Origin',(0.,0.,2.));
#4265=CARTESIAN_POINT('',(-5.,-6.12323399573677E-16,0.));
#4266=CARTESIAN_POINT('',(-5.,-6.12323399573677E-16,0.));
#4267=CARTESIAN_POINT('Origin',(0.,0.,0.));
#4268=CARTESIAN_POINT('Origin',(0.,0.,0.));
#4269=CARTESIAN_POINT('',(-10.,-1.22464679914735E-15,2.));
#4270=CARTESIAN_POINT('Origin',(0.,0.,2.));
#4271=CARTESIAN_POINT('',(-10.,-1.22464679914735E-15,0.));
#4272=CARTESIAN_POINT('',(-10.,-1.22464679914735E-15,0.));
#4273=CARTESIAN_POINT('Origin',(0.,0.,0.));
#4274=CARTESIAN_POINT('Origin',(0.,0.,2.));
#4275=CARTESIAN_POINT('Origin',(0.,0.,0.));
#4364=UNCERTAINTY_MEASURE_WITH_UNIT(LENGTH_MEASURE(0.01),#4389,
'DISTANCE_ACCURACY_VALUE',
'Maximum model space distance between geometric entities at asserted c
onnectivities');
#4366=UNCERTAINTY_MEASURE_WITH_UNIT(LENGTH_MEASURE(0.01),#4389,
'DISTANCE_ACCURACY_VALUE',
'Maximum model space distance between geometric entities at asserted c
onnectivities');
#4386=(
GEOMETRIC_REPRESENTATION_CONTEXT(3)
GLOBAL_UNCERTAINTY_ASSIGNED_CONTEXT((#4364))
GLOBAL_UNIT_ASSIGNED_CONTEXT((#4389,#4391,#4392))
REPRESENTATION_CONTEXT('','3D')
);
#4388=(
GEOMETRIC_REPRESENTATION_CONTEXT(3)
GLOBAL_UNCERTAINTY_ASSIGNED_CONTEXT((#4366))
GLOBAL_UNIT_ASSIGNED_CONTEXT((#4389,#4391,#4392))
REPRESENTATION_CONTEXT('','3D')
);
#4389=(
LENGTH_UNIT()
NAMED_UNIT(*)
SI_UNIT(.MILLI.,.METRE.)
);
#4391=(
NAMED_UNIT(*)
PLANE_ANGLE_UNIT()
SI_UNIT($,.RADIAN.)
);
#4392=(
NAMED_UNIT(*)
SI_UNIT($,.STERADIAN.)
SOLID_ANGLE_UNIT()
);
#4412=SHAPE_DEFINITION_REPRESENTATION(#4433,#4496);
#4433=PRODUCT_DEFINITION_SHAPE('',$,#4518);
#4496=SHAPE_REPRESENTATION('',(#2835),#4386);
#4498=PRODUCT_DEFINITION_CONTEXT('part definition',#4563,'design');
#4518=PRODUCT_DEFINITION('Pivot washer','Pivot washer',#4539,#4498);
#4539=PRODUCT_DEFINITION_FORMATION('',$,#4584);
#4563=APPLICATION_CONTEXT(
'Core Data for Automotive Mechanical Design Process');
#4564=PRODUCT_CONTEXT('part definition',#4563,'mechanical');
#4584=PRODUCT('Pivot washer','Pivot washer',$,(#4564));
#4598=PRESENTATION_STYLE_ASSIGNMENT((#4612));
#4612=SURFACE_STYLE_USAGE(.BOTH.,#4626);
#4626=SURFACE_SIDE_STYLE('',(#4640));
#4640=SURFACE_STYLE_FILL_AREA(#4654);
#4654=FILL_AREA_STYLE('Washer light gray',(#4668));
#4668=FILL_AREA_STYLE_COLOUR('Washer light gray',#4682);
#4682=COLOUR_RGB('Washer light gray',0.725490196078431,0.752941176470588,
0.792156862745098);
ENDSEC;
END-ISO-10303-21;
